ISO-10303-21;
HEADER;
/* Generated by software containing ST-Developer
 * from STEP Tools, Inc. (www.steptools.com) 
 */

FILE_DESCRIPTION(
/* description */ ('Compact intermittent indexer'),
/* implementation_level */ '2;1');

FILE_NAME(
/* name */ 'Foot strip (1).step',
/* time_stamp */ '2026-10-29T16:32:17-07:00',
/* author */ (''),
/* organization */ (''),
/* preprocessor_version */ 'ST-DEVELOPER v20.2',
/* originating_system */ 'Autodesk Translation Framework v15.17.0.0',
/* authorisation */ '');

FILE_SCHEMA (('AUTOMOTIVE_DESIGN { 1 0 10303 214 3 1 1 }'));
ENDSEC;

DATA;
#10=MECHANICAL_DESIGN_GEOMETRIC_PRESENTATION_REPRESENTATION('',(#259),#10837);
#211=SHAPE_REPRESENTATION_RELATIONSHIP('SRR','None',#10945,#235);
#235=ADVANCED_BREP_SHAPE_REPRESENTATION('',(#291),#10812);
#259=STYLED_ITEM('',(#11152),#291);
#291=MANIFOLD_SOLID_BREP('Body1',#5631);
#508=PLANE('',#6058);
#509=PLANE('',#6059);
#510=PLANE('',#6060);
#511=PLANE('',#6061);
#512=PLANE('',#6062);
#513=PLANE('',#6063);
#719=FACE_OUTER_BOUND('',#1094,.T.);
#720=FACE_OUTER_BOUND('',#1095,.T.);
#721=FACE_OUTER_BOUND('',#1096,.T.);
#722=FACE_OUTER_BOUND('',#1097,.T.);
#723=FACE_OUTER_BOUND('',#1098,.T.);
#724=FACE_OUTER_BOUND('',#1099,.T.);
#1094=EDGE_LOOP('',(#3960,#3961,#3962,#3963));
#1095=EDGE_LOOP('',(#3964,#3965,#3966,#3967));
#1096=EDGE_LOOP('',(#3968,#3969,#3970,#3971));
#1097=EDGE_LOOP('',(#3972,#3973,#3974,#3975));
#1098=EDGE_LOOP('',(#3976,#3977,#3978,#3979));
#1099=EDGE_LOOP('',(#3980,#3981,#3982,#3983));
#1498=LINE('',#8851,#1856);
#1499=LINE('',#8853,#1857);
#1500=LINE('',#8855,#1858);
#1501=LINE('',#8856,#1859);
#1502=LINE('',#8859,#1860);
#1503=LINE('',#8861,#1861);
#1504=LINE('',#8862,#1862);
#1505=LINE('',#8865,#1863);
#1506=LINE('',#8867,#1864);
#1507=LINE('',#8868,#1865);
#1508=LINE('',#8870,#1866);
#1509=LINE('',#8871,#1867);
#1856=VECTOR('',#6994,1.);
#1857=VECTOR('',#6995,1.);
#1858=VECTOR('',#6996,1.);
#1859=VECTOR('',#6997,1.);
#1860=VECTOR('',#7000,1.);
#1861=VECTOR('',#7001,1.);
#1862=VECTOR('',#7002,1.);
#1863=VECTOR('',#7005,1.);
#1864=VECTOR('',#7006,1.);
#1865=VECTOR('',#7007,1.);
#1866=VECTOR('',#7010,1.);
#1867=VECTOR('',#7011,1.);
#2566=VERTEX_POINT('',#8849);
#2567=VERTEX_POINT('',#8850);
#2568=VERTEX_POINT('',#8852);
#2569=VERTEX_POINT('',#8854);
#2570=VERTEX_POINT('',#8858);
#2571=VERTEX_POINT('',#8860);
#2572=VERTEX_POINT('',#8864);
#2573=VERTEX_POINT('',#8866);
#3102=EDGE_CURVE('',#2566,#2567,#1498,.T.);
#3103=EDGE_CURVE('',#2567,#2568,#1499,.T.);
#3104=EDGE_CURVE('',#2569,#2568,#1500,.T.);
#3105=EDGE_CURVE('',#2566,#2569,#1501,.T.);
#3106=EDGE_CURVE('',#2570,#2566,#1502,.T.);
#3107=EDGE_CURVE('',#2571,#2569,#1503,.T.);
#3108=EDGE_CURVE('',#2570,#2571,#1504,.T.);
#3109=EDGE_CURVE('',#2572,#2570,#1505,.T.);
#3110=EDGE_CURVE('',#2573,#2571,#1506,.T.);
#3111=EDGE_CURVE('',#2572,#2573,#1507,.T.);
#3112=EDGE_CURVE('',#2567,#2572,#1508,.T.);
#3113=EDGE_CURVE('',#2568,#2573,#1509,.T.);
#3960=ORIENTED_EDGE('',*,*,#3102,.T.);
#3961=ORIENTED_EDGE('',*,*,#3103,.T.);
#3962=ORIENTED_EDGE('',*,*,#3104,.F.);
#3963=ORIENTED_EDGE('',*,*,#3105,.F.);
#3964=ORIENTED_EDGE('',*,*,#3106,.T.);
#3965=ORIENTED_EDGE('',*,*,#3105,.T.);
#3966=ORIENTED_EDGE('',*,*,#3107,.F.);
#3967=ORIENTED_EDGE('',*,*,#3108,.F.);
#3968=ORIENTED_EDGE('',*,*,#3109,.T.);
#3969=ORIENTED_EDGE('',*,*,#3108,.T.);
#3970=ORIENTED_EDGE('',*,*,#3110,.F.);
#3971=ORIENTED_EDGE('',*,*,#3111,.F.);
#3972=ORIENTED_EDGE('',*,*,#3112,.T.);
#3973=ORIENTED_EDGE('',*,*,#3111,.T.);
#3974=ORIENTED_EDGE('',*,*,#3113,.F.);
#3975=ORIENTED_EDGE('',*,*,#3103,.F.);
#3976=ORIENTED_EDGE('',*,*,#3113,.T.);
#3977=ORIENTED_EDGE('',*,*,#3110,.T.);
#3978=ORIENTED_EDGE('',*,*,#3107,.T.);
#3979=ORIENTED_EDGE('',*,*,#3104,.T.);
#3980=ORIENTED_EDGE('',*,*,#3112,.F.);
#3981=ORIENTED_EDGE('',*,*,#3102,.F.);
#3982=ORIENTED_EDGE('',*,*,#3106,.F.);
#3983=ORIENTED_EDGE('',*,*,#3109,.F.);
#5362=ADVANCED_FACE('',(#719),#508,.T.);
#5363=ADVANCED_FACE('',(#720),#509,.T.);
#5364=ADVANCED_FACE('',(#721),#510,.T.);
#5365=ADVANCED_FACE('',(#722),#511,.T.);
#5366=ADVANCED_FACE('',(#723),#512,.T.);
#5367=ADVANCED_FACE('',(#724),#513,.F.);
#5631=CLOSED_SHELL('',(#5362,#5363,#5364,#5365,#5366,#5367));
#6057=AXIS2_PLACEMENT_3D('',#8847,#6990,#6991);
#6058=AXIS2_PLACEMENT_3D('',#8848,#6992,#6993);
#6059=AXIS2_PLACEMENT_3D('',#8857,#6998,#6999);
#6060=AXIS2_PLACEMENT_3D('',#8863,#7003,#7004);
#6061=AXIS2_PLACEMENT_3D('',#8869,#7008,#7009);
#6062=AXIS2_PLACEMENT_3D('',#8872,#7012,#7013);
#6063=AXIS2_PLACEMENT_3D('',#8873,#7014,#7015);
#6990=DIRECTION('axis',(0.,0.,1.));
#6991=DIRECTION('refdir',(1.,0.,0.));
#6992=DIRECTION('center_axis',(0.,1.,0.));
#6993=DIRECTION('ref_axis',(-1.,0.,0.));
#6994=DIRECTION('',(-1.,0.,0.));
#6995=DIRECTION('',(0.,0.,1.));
#6996=DIRECTION('',(-1.,0.,0.));
#6997=DIRECTION('',(0.,0.,1.));
#6998=DIRECTION('center_axis',(1.,0.,0.));
#6999=DIRECTION('ref_axis',(0.,1.,0.));
#7000=DIRECTION('',(0.,1.,0.));
#7001=DIRECTION('',(0.,1.,0.));
#7002=DIRECTION('',(0.,0.,1.));
#7003=DIRECTION('center_axis',(0.,-1.,0.));
#7004=DIRECTION('ref_axis',(1.,0.,0.));
#7005=DIRECTION('',(1.,0.,0.));
#7006=DIRECTION('',(1.,0.,0.));
#7007=DIRECTION('',(0.,0.,1.));
#7008=DIRECTION('center_axis',(-1.,0.,0.));
#7009=DIRECTION('ref_axis',(0.,-1.,0.));
#7010=DIRECTION('',(0.,-1.,0.));
#7011=DIRECTION('',(0.,-1.,0.));
#7012=DIRECTION('center_axis',(0.,0.,1.));
#7013=DIRECTION('ref_axis',(1.,0.,0.));
#7014=DIRECTION('center_axis',(0.,0.,1.));
#7015=DIRECTION('ref_axis',(1.,0.,0.));
#8847=CARTESIAN_POINT('',(0.,0.,0.));
#8848=CARTESIAN_POINT('Origin',(8.,4.,-0.6));
#8849=CARTESIAN_POINT('',(8.,4.,-0.6));
#8850=CARTESIAN_POINT('',(-3.5,4.,-0.6));
#8851=CARTESIAN_POINT('',(8.,4.,-0.6));
#8852=CARTESIAN_POINT('',(-3.5,4.,0.));
#8853=CARTESIAN_POINT('',(-3.5,4.,-0.6));
#8854=CARTESIAN_POINT('',(8.,4.,0.));
#8855=CARTESIAN_POINT('',(8.,4.,0.));
#8856=CARTESIAN_POINT('',(8.,4.,-0.6));
#8857=CARTESIAN_POINT('Origin',(8.,3.2,-0.6));
#8858=CARTESIAN_POINT('',(8.,3.2,-0.6));
#8859=CARTESIAN_POINT('',(8.,3.2,-0.6));
#8860=CARTESIAN_POINT('',(8.,3.2,0.));
#8861=CARTESIAN_POINT('',(8.,3.2,0.));
#8862=CARTESIAN_POINT('',(8.,3.2,-0.6));
#8863=CARTESIAN_POINT('Origin',(-3.5,3.2,-0.6));
#8864=CARTESIAN_POINT('',(-3.5,3.2,-0.6));
#8865=CARTESIAN_POINT('',(-3.5,3.2,-0.6));
#8866=CARTESIAN_POINT('',(-3.5,3.2,0.));
#8867=CARTESIAN_POINT('',(-3.5,3.2,0.));
#8868=CARTESIAN_POINT('',(-3.5,3.2,-0.6));
#8869=CARTESIAN_POINT('Origin',(-3.5,4.,-0.6));
#8870=CARTESIAN_POINT('',(-3.5,4.,-0.6));
#8871=CARTESIAN_POINT('',(-3.5,4.,0.));
#8872=CARTESIAN_POINT('Origin',(2.25,3.6,0.));
#8873=CARTESIAN_POINT('Origin',(2.25,3.6,-0.6));
#10782=UNCERTAINTY_MEASURE_WITH_UNIT(LENGTH_MEASURE(0.001),#10838,
'DISTANCE_ACCURACY_VALUE',
'Maximum model space distance between geometric entities at asserted c
onnectivities');
#10807=UNCERTAINTY_MEASURE_WITH_UNIT(LENGTH_MEASURE(0.001),#10838,
'DISTANCE_ACCURACY_VALUE',
'Maximum model space distance between geometric entities at asserted c
onnectivities');
#10812=(
GEOMETRIC_REPRESENTATION_CONTEXT(3)
GLOBAL_UNCERTAINTY_ASSIGNED_CONTEXT((#10782))
GLOBAL_UNIT_ASSIGNED_CONTEXT((#10838,#10840,#10841))
REPRESENTATION_CONTEXT('','3D')
);
#10837=(
GEOMETRIC_REPRESENTATION_CONTEXT(3)
GLOBAL_UNCERTAINTY_ASSIGNED_CONTEXT((#10807))
GLOBAL_UNIT_ASSIGNED_CONTEXT((#10838,#10840,#10841))
REPRESENTATION_CONTEXT('','3D')
);
#10838=(
LENGTH_UNIT()
NAMED_UNIT(*)
SI_UNIT(.CENTI.,.METRE.)
);
#10840=(
NAMED_UNIT(*)
PLANE_ANGLE_UNIT()
SI_UNIT($,.RADIAN.)
);
#10841=(
NAMED_UNIT(*)
SI_UNIT($,.STERADIAN.)
SOLID_ANGLE_UNIT()
);
#10846=SHAPE_DEFINITION_REPRESENTATION(#10875,#10945);
#10875=PRODUCT_DEFINITION_SHAPE('',$,#10975);
#10945=SHAPE_REPRESENTATION('',(#6057),#10812);
#10970=PRODUCT_DEFINITION_CONTEXT('part definition',#11059,'design');
#10975=PRODUCT_DEFINITION('Foot strip (1)','Foot strip (1)',#11004,#10970);
#11004=PRODUCT_DEFINITION_FORMATION('',$,#11065);
#11059=APPLICATION_CONTEXT(
'Core Data for Automotive Mechanical Design Process');
#11060=PRODUCT_CONTEXT('part definition',#11059,'mechanical');
#11065=PRODUCT('Foot strip (1)','Foot strip (1)','Foot strip (1)',(#11060));
#11146=COLOUR_RGB('Light Blue',0.38,0.62,0.78);
#11147=FILL_AREA_STYLE_COLOUR('',#11146);
#11148=FILL_AREA_STYLE('',(#11147));
#11149=SURFACE_STYLE_FILL_AREA(#11148);
#11150=SURFACE_SIDE_STYLE('',(#11149));
#11151=SURFACE_STYLE_USAGE(.BOTH.,#11150);
#11152=PRESENTATION_STYLE_ASSIGNMENT((#11151));
ENDSEC;
END-ISO-10303-21;
